ISO-10303-21;
HEADER;
FILE_DESCRIPTION (('STEP AP214'),
    '1' );
FILE_NAME ('socket head cap screw_iso_ISO 4762 M10 x 16 - 16N.step',
    '2026-10-26T22:46:44',
    ( '' ),
    ( '' ),
    'SwSTEP 2.0',
    'SolidWorks 2025',
    '' );
FILE_SCHEMA (( 'AUTOMOTIVE_DESIGN' ));
ENDSEC;

DATA;
#18=AXIS2_PLACEMENT_3D ( 'NONE', #4792, #10950, #15638 ) ;
#79=CARTESIAN_POINT ( 'NONE',  ( 25.17200000000003612, 0.000000000000000000, 0.000000000000000000 ) ) ;
#98=EDGE_LOOP ( 'NONE', ( #990, #8694, #13068, #17263 ) ) ;
#121=DIRECTION ( 'NONE',  ( -0.7071067811865331398, 8.659560562355110352E-17, -0.7071067811865620056 ) ) ;
#172=LINE ( 'NONE', #6717, #1739 ) ;
#190=CARTESIAN_POINT ( 'NONE',  ( 5.000000000000000000, -4.685197434473809430, 6.071532165918824830E-15 ) ) ;
#239=ORIENTED_EDGE ( 'NONE', *, *, #5233, .T. ) ;
#240=ORIENTED_EDGE ( 'NONE', *, *, #10844, .T. ) ;
#246=DIRECTION ( 'NONE',  ( 1.000000000000000000, 0.000000000000000000, 0.000000000000000000 ) ) ;
#279=VERTEX_POINT ( 'NONE', #5885 ) ;
#293=ADVANCED_FACE ( 'NONE', ( #8966 ), #1343, .F. ) ;
#302=CARTESIAN_POINT ( 'NONE',  ( 5.000000000000000000, 4.685197434473812983, -6.938893903907228378E-15 ) ) ;
#390=LINE ( 'NONE', #1771, #19960 ) ;
#393=ADVANCED_FACE ( 'NONE', ( #3140 ), #14498, .F. ) ;
#454=ORIENTED_EDGE ( 'NONE', *, *, #14721, .F. ) ;
#456=VERTEX_POINT ( 'NONE', #6830 ) ;
#483=CARTESIAN_POINT ( 'NONE',  ( 1.500000000000001332, 0.000000000000000000, 0.000000000000000000 ) ) ;
#485=ORIENTED_EDGE ( 'NONE', *, *, #15962, .F. ) ;
#488=( LENGTH_UNIT ( ) NAMED_UNIT ( * ) SI_UNIT ( .MILLI., .METRE. ) );
#519=CARTESIAN_POINT ( 'NONE',  ( 5.000000000000000000, 4.685197434473812983, -6.938893903907228378E-15 ) ) ;
#522=PLANE ( 'NONE',  #19314 ) ;
#523=CARTESIAN_POINT ( 'NONE',  ( -31.74999999999995737, 6.123233995736767268E-16, -5.000000000000000888 ) ) ;
#525=ORIENTED_EDGE ( 'NONE', *, *, #20015, .F. ) ;
#529=CARTESIAN_POINT ( 'NONE',  ( 26.00000000000000355, 0.000000000000000000, 4.171999999999999709 ) ) ;
#530=DIRECTION ( 'NONE',  ( -1.000000000000000000, -0.000000000000000000, -0.000000000000000000 ) ) ;
#545=PLANE ( 'NONE',  #2441 ) ;
#555=VECTOR ( 'NONE', #8498, 999.9999999999998863 ) ;
#608=AXIS2_PLACEMENT_3D ( 'NONE', #16458, #246, #12770 ) ;
#623=CARTESIAN_POINT ( 'NONE',  ( 5.000000000000000000, 7.027796151710712813, -4.057500000000007212 ) ) ;
#625=DIRECTION ( 'NONE',  ( -1.000000000000000000, -0.000000000000000000, -0.000000000000000000 ) ) ;
#634=AXIS2_PLACEMENT_3D ( 'NONE', #2156, #10183, #5206 ) ;
#658=FACE_OUTER_BOUND ( 'NONE', #17928, .T. ) ;
#731=CONICAL_SURFACE ( 'NONE', #20347, 4.057500000000000107, 1.047197551196593857 ) ;
#807=DIRECTION ( 'NONE',  ( 0.000000000000000000, 0.000000000000000000, -1.000000000000000000 ) ) ;
#822=ADVANCED_FACE ( 'NONE', ( #658 ), #1575, .T. ) ;
#824=EDGE_CURVE ( 'NONE', #14364, #18356, #5520, .T. ) ;
#935=CARTESIAN_POINT ( 'NONE',  ( 25.17200000000003612, 0.000000000000000000, 0.000000000000000000 ) ) ;
#990=ORIENTED_EDGE ( 'NONE', *, *, #7291, .F. ) ;
#1032=VERTEX_POINT ( 'NONE', #14138 ) ;
#1065=DIRECTION ( 'NONE',  ( 0.000000000000000000, 0.000000000000000000, 1.000000000000000000 ) ) ;
#1066=CARTESIAN_POINT ( 'NONE',  ( 10.00000000000000178, 0.000000000000000000, 8.000000000000000000 ) ) ;
#1070=LINE ( 'NONE', #12420, #20824 ) ;
#1083=AXIS2_PLACEMENT_3D ( 'NONE', #8939, #14269, #20487 ) ;
#1119=SHAPE_REPRESENTATION_RELATIONSHIP ( 'NONE' , 'NONE' ,  #8398, #1482 ) ;
#1169=DIRECTION ( 'NONE',  ( 1.000000000000000000, 0.000000000000000000, 0.000000000000000000 ) ) ;
#1188=PRODUCT_CONTEXT ( 'NONE', #7405, 'mechanical' ) ;
#1207=EDGE_CURVE ( 'NONE', #9907, #14800, #4883, .T. ) ;
#1216=VECTOR ( 'NONE', #2994, 1000.000000000000114 ) ;
#1227=EDGE_CURVE ( 'NONE', #14364, #279, #19497, .T. ) ;
#1230=CIRCLE ( 'NONE', #1557, 4.057500000000000107 ) ;
#1232=AXIS2_PLACEMENT_3D ( 'NONE', #4635, #11100, #8006 ) ;
#1239=LINE ( 'NONE', #15772, #8678 ) ;
#1251=FACE_OUTER_BOUND ( 'NONE', #16643, .T. ) ;
#1260=ORIENTED_EDGE ( 'NONE', *, *, #15399, .F. ) ;
#1274=DIRECTION ( 'NONE',  ( 0.000000000000000000, 0.000000000000000000, 1.000000000000000000 ) ) ;
#1277=LINE ( 'NONE', #9721, #2686 ) ;
#1278=DIRECTION ( 'NONE',  ( 0.000000000000000000, 0.000000000000000000, 1.000000000000000000 ) ) ;
#1319=PRODUCT_DEFINITION_CONTEXT ( 'detailed design', #13525, 'design' ) ;
#1331=CARTESIAN_POINT ( 'NONE',  ( 5.000000000000000000, -2.342598717236899386, 4.057500000000001883 ) ) ;
#1336=FACE_OUTER_BOUND ( 'NONE', #14267, .T. ) ;
#1343=PLANE ( 'NONE',  #10342 ) ;
#1351=( NAMED_UNIT ( * ) SI_UNIT ( $, .STERADIAN. ) SOLID_ANGLE_UNIT ( ) );
#1389=EDGE_CURVE ( 'NONE', #2300, #18834, #20107, .T. ) ;
#1398=ADVANCED_FACE ( 'NONE', ( #10473 ), #4344, .T. ) ;
#1407=CARTESIAN_POINT ( 'NONE',  ( 5.000000000000000000, -2.342598717236910932, -4.057499999999996554 ) ) ;
#1419=DIRECTION ( 'NONE',  ( 0.000000000000000000, 0.000000000000000000, -1.000000000000000000 ) ) ;
#1437=CARTESIAN_POINT ( 'NONE',  ( 5.000000000000000000, 2.342598717236900718, -4.057500000000001883 ) ) ;
#1458=PLANE ( 'NONE',  #17046 ) ;
#1482=ADVANCED_BREP_SHAPE_REPRESENTATION ( '', ( #10492, #18233 ), #11452 ) ;
#1499=SHAPE_DEFINITION_REPRESENTATION ( #14006, #8398 ) ;
#1539=DIRECTION ( 'NONE',  ( 0.000000000000000000, 0.5000000000000009992, 0.8660254037844380415 ) ) ;
#1557=AXIS2_PLACEMENT_3D ( 'NONE', #20567, #14134, #9533 ) ;
#1575=CONICAL_SURFACE ( 'NONE', #10354, 4.171999999999999709, 0.7853981633974687071 ) ;
#1629=LINE ( 'NONE', #14581, #3324 ) ;
#1645=EDGE_CURVE ( 'NONE', #16948, #3078, #11718, .T. ) ;
#1663=DIRECTION ( 'NONE',  ( -0.000000000000000000, 0.000000000000000000, 1.000000000000000000 ) ) ;
#1664=EDGE_CURVE ( 'NONE', #18303, #11033, #10531, .T. ) ;
#1711=AXIS2_PLACEMENT_3D ( 'NONE', #5832, #12327, #4257 ) ;
#1724=VECTOR ( 'NONE', #9757, 1000.000000000000000 ) ;
#1730=UNCERTAINTY_MEASURE_WITH_UNIT (LENGTH_MEASURE( 1.000000000000000082E-05 ), #2942, 'distance_accuracy_value', 'NONE');
#1734=ADVANCED_FACE ( 'NONE', ( #7037 ), #2076, .T. ) ;
#1739=VECTOR ( 'NONE', #13110, 1000.000000000000114 ) ;
#1771=CARTESIAN_POINT ( 'NONE',  ( 5.000000000000000000, 2.342598717236900718, -4.057500000000001883 ) ) ;
#1776=EDGE_LOOP ( 'NONE', ( #10462, #16999, #6651, #485, #4901 ) ) ;
#1835=EDGE_LOOP ( 'NONE', ( #7186, #6081, #4763, #7873, #7940 ) ) ;
#1839=DIRECTION ( 'NONE',  ( 0.000000000000000000, -1.000000000000000000, 1.110768649713242108E-15 ) ) ;
#1841=LINE ( 'NONE', #19841, #8681 ) ;
#1886=CARTESIAN_POINT ( 'NONE',  ( 0.000000000000000000, -2.342598717236899386, 4.057500000000001883 ) ) ;
#1952=DIRECTION ( 'NONE',  ( 0.000000000000000000, 0.000000000000000000, -1.000000000000000000 ) ) ;
#1953=ORIENTED_EDGE ( 'NONE', *, *, #4597, .T. ) ;
#2012=ORIENTED_EDGE ( 'NONE', *, *, #2100, .T. ) ;
#2045=DIRECTION ( 'NONE',  ( -1.000000000000000000, -0.000000000000000000, -0.000000000000000000 ) ) ;
#2076=CYLINDRICAL_SURFACE ( 'NONE', #2530, 8.000000000000000000 ) ;
#2100=EDGE_CURVE ( 'NONE', #3078, #10779, #19842, .T. ) ;
#2156=CARTESIAN_POINT ( 'NONE',  ( 10.00000000000000178, 0.000000000000000000, 0.000000000000000000 ) ) ;
#2176=DIRECTION ( 'NONE',  ( -1.000000000000000000, -0.000000000000000000, -0.000000000000000000 ) ) ;
#2186=ORIENTED_EDGE ( 'NONE', *, *, #16687, .T. ) ;
#2210=CONICAL_SURFACE ( 'NONE', #20476, 4.057500000000000107, 1.047197551196593857 ) ;
#2220=ORIENTED_EDGE ( 'NONE', *, *, #16687, .F. ) ;
#2300=VERTEX_POINT ( 'NONE', #16990 ) ;
#2403=EDGE_CURVE ( 'NONE', #18303, #10779, #16141, .T. ) ;
#2425=CARTESIAN_POINT ( 'NONE',  ( 9.999999999999998224, 0.000000000000000000, 0.000000000000000000 ) ) ;
#2441=AXIS2_PLACEMENT_3D ( 'NONE', #6995, #10484, #12205 ) ;
#2469=CARTESIAN_POINT ( 'NONE',  ( 5.000000000000000000, -4.685197434473809430, 6.071532165918824830E-15 ) ) ;
#2519=DIRECTION ( 'NONE',  ( -1.000000000000000000, -0.000000000000000000, -0.000000000000000000 ) ) ;
#2530=AXIS2_PLACEMENT_3D ( 'NONE', #10099, #10210, #3755 ) ;
#2540=EDGE_CURVE ( 'NONE', #456, #10779, #9612, .T. ) ;
#2686=VECTOR ( 'NONE', #3066, 1000.000000000000114 ) ;
#2730=CARTESIAN_POINT ( 'NONE',  ( 5.000000000000000000, 0.000000000000000000, 0.000000000000000000 ) ) ;
#2820=FACE_OUTER_BOUND ( 'NONE', #8759, .T. ) ;
#2845=DIRECTION ( 'NONE',  ( 0.000000000000000000, 0.000000000000000000, 1.000000000000000000 ) ) ;
#2862=FACE_OUTER_BOUND ( 'NONE', #18703, .T. ) ;
#2877=ADVANCED_FACE ( 'NONE', ( #13863 ), #4099, .T. ) ;
#2878=VERTEX_POINT ( 'NONE', #19440 ) ;
#2895=AXIS2_PLACEMENT_3D ( 'NONE', #6507, #9411, #1278 ) ;
#2926=VECTOR ( 'NONE', #625, 1000.000000000000000 ) ;
#2935=DIRECTION ( 'NONE',  ( 0.000000000000000000, 0.000000000000000000, 1.000000000000000000 ) ) ;
#2942=( LENGTH_UNIT ( ) NAMED_UNIT ( * ) SI_UNIT ( .MILLI., .METRE. ) );
#2994=DIRECTION ( 'NONE',  ( 0.000000000000000000, -0.5000000000000009992, -0.8660254037844380415 ) ) ;
#3064=CARTESIAN_POINT ( 'NONE',  ( 26.00000000000000355, 4.171999999999999709, 0.000000000000000000 ) ) ;
#3066=DIRECTION ( 'NONE',  ( 0.000000000000000000, 0.4999999999999985012, -0.8660254037844394848 ) ) ;
#3078=VERTEX_POINT ( 'NONE', #3541 ) ;
#3082=ORIENTED_EDGE ( 'NONE', *, *, #3899, .T. ) ;
#3140=FACE_OUTER_BOUND ( 'NONE', #1776, .T. ) ;
#3167=CARTESIAN_POINT ( 'NONE',  ( 5.000000000000000000, 3.513898075855363068, 2.028749999999995168 ) ) ;
#3168=ADVANCED_FACE ( 'NONE', ( #3640 ), #12247, .T. ) ;
#3183=VERTEX_POINT ( 'NONE', #7032 ) ;
#3191=ORIENTED_EDGE ( 'NONE', *, *, #16876, .F. ) ;
#3200=FACE_OUTER_BOUND ( 'NONE', #3619, .T. ) ;
#3245=FACE_BOUND ( 'NONE', #11126, .T. ) ;
#3280=EDGE_CURVE ( 'NONE', #279, #16948, #6478, .T. ) ;
#3324=VECTOR ( 'NONE', #1839, 1000.000000000000000 ) ;
#3330=DIRECTION ( 'NONE',  ( -1.000000000000000000, -0.000000000000000000, -0.000000000000000000 ) ) ;
#3337=EDGE_LOOP ( 'NONE', ( #9563, #18671, #15643, #10214 ) ) ;
#3350=CARTESIAN_POINT ( 'NONE',  ( 5.000000000000000000, 4.685197434473812983, -6.938893903907228378E-15 ) ) ;
#3382=EDGE_CURVE ( 'NONE', #7667, #279, #5467, .T. ) ;
#3475=ADVANCED_FACE ( 'NONE', ( #20195 ), #8851, .F. ) ;
#3541=CARTESIAN_POINT ( 'NONE',  ( 5.000000000000000000, 2.342598717236913153, 4.057499999999995666 ) ) ;
#3619=EDGE_LOOP ( 'NONE', ( #16905, #16608, #240, #2220 ) ) ;
#3634=CARTESIAN_POINT ( 'NONE',  ( 1.500000000000001332, 0.000000000000000000, 0.000000000000000000 ) ) ;
#3640=FACE_OUTER_BOUND ( 'NONE', #10474, .T. ) ;
#3662=ORIENTED_EDGE ( 'NONE', *, *, #1664, .T. ) ;
#3687=ORIENTED_EDGE ( 'NONE', *, *, #17308, .T. ) ;
#3697=EDGE_CURVE ( 'NONE', #20933, #1032, #7793, .T. ) ;
#3755=DIRECTION ( 'NONE',  ( 0.000000000000000000, 0.000000000000000000, 1.000000000000000000 ) ) ;
#3771=ORIENTED_EDGE ( 'NONE', *, *, #1645, .F. ) ;
#3820=CARTESIAN_POINT ( 'NONE',  ( 5.000000000000000000, -2.342598717236899386, 4.057500000000001883 ) ) ;
#3875=ORIENTED_EDGE ( 'NONE', *, *, #15962, .T. ) ;
#3899=EDGE_CURVE ( 'NONE', #9907, #19392, #12200, .T. ) ;
#3946=CARTESIAN_POINT ( 'NONE',  ( 5.000000000000000000, 2.342598717236913153, 4.057499999999995666 ) ) ;
#3971=CARTESIAN_POINT ( 'NONE',  ( 0.000000000000000000, 4.685197434473812983, -6.938893903907228378E-15 ) ) ;
#4005=FACE_OUTER_BOUND ( 'NONE', #18195, .T. ) ;
#4037=DIRECTION ( 'NONE',  ( 0.000000000000000000, -1.110768649713242108E-15, -1.000000000000000000 ) ) ;
#4043=EDGE_CURVE ( 'NONE', #10411, #18303, #14990, .T. ) ;
#4051=CIRCLE ( 'NONE', #19949, 5.000000000000000888 ) ;
#4073=CARTESIAN_POINT ( 'NONE',  ( 5.000000000000000000, 4.685197434473812983, -6.938893903907228378E-15 ) ) ;
#4099=CYLINDRICAL_SURFACE ( 'NONE', #15307, 5.000000000000000888 ) ;
#4116=AXIS2_PLACEMENT_3D ( 'NONE', #7783, #14288, #12685 ) ;
#4122=CIRCLE ( 'NONE', #12588, 8.000000000000000000 ) ;
#4158=VERTEX_POINT ( 'NONE', #11893 ) ;
#4194=CARTESIAN_POINT ( 'NONE',  ( 5.000000000000000000, 7.027796151710712813, -4.057500000000007212 ) ) ;
#4257=DIRECTION ( 'NONE',  ( 0.000000000000000000, 0.5000000000000014433, 0.8660254037844379305 ) ) ;
#4281=VERTEX_POINT ( 'NONE', #6004 ) ;
#4325=CIRCLE ( 'NONE', #10049, 4.171999999999999709 ) ;
#4344=CYLINDRICAL_SURFACE ( 'NONE', #15064, 8.000000000000000000 ) ;
#4365=ORIENTED_EDGE ( 'NONE', *, *, #17308, .F. ) ;
#4434=ORIENTED_EDGE ( 'NONE', *, *, #14083, .F. ) ;
#4460=DIRECTION ( 'NONE',  ( 0.000000000000000000, 1.000000000000000000, -1.295896757998782163E-15 ) ) ;
#4510=DIRECTION ( 'NONE',  ( 1.000000000000000000, 0.000000000000000000, 0.000000000000000000 ) ) ;
#4531=CARTESIAN_POINT ( 'NONE',  ( 0.000000000000000000, 0.000000000000000000, 0.000000000000000000 ) ) ;
#4558=DIRECTION ( 'NONE',  ( 0.000000000000000000, 0.000000000000000000, 1.000000000000000000 ) ) ;
#4566=ORIENTED_EDGE ( 'NONE', *, *, #14196, .T. ) ;
#4597=EDGE_CURVE ( 'NONE', #9257, #7667, #7182, .T. ) ;
#4608=LINE ( 'NONE', #1437, #15842 ) ;
#4628=ADVANCED_FACE ( 'NONE', ( #13749 ), #5057, .F. ) ;
#4635=CARTESIAN_POINT ( 'NONE',  ( 5.000000000000000000, 0.000000000000000000, 0.000000000000000000 ) ) ;
#4708=DIRECTION ( 'NONE',  ( 0.000000000000000000, -1.000000000000000000, 1.110768649713242108E-15 ) ) ;
#4739=EDGE_CURVE ( 'NONE', #16434, #2300, #4051, .T. ) ;
#4763=ORIENTED_EDGE ( 'NONE', *, *, #3280, .T. ) ;
#4778=EDGE_LOOP ( 'NONE', ( #3662, #18094, #1260, #16661, #6660 ) ) ;
#4782=CARTESIAN_POINT ( 'NONE',  ( 0.000000000000000000, 4.685197434473812983, -6.938893903907228378E-15 ) ) ;
#4792=CARTESIAN_POINT ( 'NONE',  ( 26.00000000000000355, 0.000000000000000000, 0.000000000000000000 ) ) ;
#4795=DIRECTION ( 'NONE',  ( 1.000000000000000000, 0.000000000000000000, 0.000000000000000000 ) ) ;
#4819=FACE_OUTER_BOUND ( 'NONE', #15044, .T. ) ;
#4866=VECTOR ( 'NONE', #13899, 1000.000000000000000 ) ;
#4883=LINE ( 'NONE', #9742, #15383 ) ;
#4901=ORIENTED_EDGE ( 'NONE', *, *, #7247, .T. ) ;
#5006=VECTOR ( 'NONE', #7101, 1000.000000000000000 ) ;
#5038=ADVANCED_FACE ( 'NONE', ( #10276 ), #15411, .F. ) ;
#5057=TOROIDAL_SURFACE ( 'NONE', #15577, 5.400000000000001243, 0.4000000000000000222 ) ;
#5177=ORIENTED_EDGE ( 'NONE', *, *, #15347, .F. ) ;
#5197=ORIENTED_EDGE ( 'NONE', *, *, #16779, .T. ) ;
#5206=DIRECTION ( 'NONE',  ( 0.000000000000000000, 0.000000000000000000, 1.000000000000000000 ) ) ;
#5208=DIRECTION ( 'NONE',  ( -1.000000000000000000, -0.000000000000000000, -0.000000000000000000 ) ) ;
#5213=FACE_OUTER_BOUND ( 'NONE', #18739, .T. ) ;
#5233=EDGE_CURVE ( 'NONE', #19392, #16971, #16132, .T. ) ;
#5275=VECTOR ( 'NONE', #15466, 1000.000000000000000 ) ;
#5379=CYLINDRICAL_SURFACE ( 'NONE', #15123, 5.000000000000000888 ) ;
#5434=DIRECTION ( 'NONE',  ( 0.000000000000000000, -0.4999999999999987232, 0.8660254037844393737 ) ) ;
#5467=CIRCLE ( 'NONE', #10903, 4.057500000000000107 ) ;
#5520=LINE ( 'NONE', #18154, #555 ) ;
#5593=LINE ( 'NONE', #7296, #10729 ) ;
#5600=EDGE_LOOP ( 'NONE', ( #11772, #10645, #11553, #20799, #12144, #9733 ) ) ;
#5629=EDGE_CURVE ( 'NONE', #13470, #18707, #11888, .T. ) ;
#5640=EDGE_LOOP ( 'NONE', ( #10838, #7014, #11294 ) ) ;
#5741=ORIENTED_EDGE ( 'NONE', *, *, #10661, .T. ) ;
#5743=PLANE ( 'NONE',  #7162 ) ;
#5745=ORIENTED_EDGE ( 'NONE', *, *, #18305, .F. ) ;
#5788=EDGE_CURVE ( 'NONE', #1032, #20933, #4122, .T. ) ;
#5789=AXIS2_PLACEMENT_3D ( 'NONE', #483, #2176, #6922 ) ;
#5832=CARTESIAN_POINT ( 'NONE',  ( 5.000000000000000000, 4.685197434473812983, -6.938893903907228378E-15 ) ) ;
#5833=CARTESIAN_POINT ( 'NONE',  ( 5.000000000000000000, 2.342598717236900718, -4.057500000000001883 ) ) ;
#5885=CARTESIAN_POINT ( 'NONE',  ( 5.000000000000000000, 5.258101095580057891E-15, 4.057499999999999218 ) ) ;
#5893=VECTOR ( 'NONE', #5208, 1000.000000000000000 ) ;
#5966=CARTESIAN_POINT ( 'NONE',  ( 5.000000000000000000, -2.342598717236899386, 4.057500000000001883 ) ) ;
#6004=CARTESIAN_POINT ( 'NONE',  ( 5.000000000000000000, -2.342598717236899386, 4.057500000000001883 ) ) ;
#6065=CARTESIAN_POINT ( 'NONE',  ( 5.000000000000000000, -4.685197434473809430, 6.071532165918824830E-15 ) ) ;
#6081=ORIENTED_EDGE ( 'NONE', *, *, #1227, .T. ) ;
#6119=AXIS2_PLACEMENT_3D ( 'NONE', #2425, #12290, #13767 ) ;
#6135=CIRCLE ( 'NONE', #6119, 5.400000000000001243 ) ;
#6196=CARTESIAN_POINT ( 'NONE',  ( 1.500000000000001332, 0.000000000000000000, 6.500000000000000888 ) ) ;
#6252=ADVANCED_FACE ( 'NONE', ( #3200 ), #17653, .T. ) ;
#6348=CARTESIAN_POINT ( 'NONE',  ( 10.40000000000000036, 0.000000000000000000, 5.000000000000000888 ) ) ;
#6354=ADVANCED_FACE ( 'NONE', ( #16660 ), #545, .F. ) ;
#6422=DIRECTION ( 'NONE',  ( 0.000000000000000000, 0.000000000000000000, 1.000000000000000000 ) ) ;
#6445=CARTESIAN_POINT ( 'NONE',  ( 5.000000000000000000, 4.685197434473812983, -6.938893903907228378E-15 ) ) ;
#6464=ORIENTED_EDGE ( 'NONE', *, *, #16876, .T. ) ;
#6478=CIRCLE ( 'NONE', #10543, 4.057500000000000107 ) ;
#6507=CARTESIAN_POINT ( 'NONE',  ( 26.00000000000000355, 0.000000000000000000, 0.000000000000000000 ) ) ;
#6516=PLANE ( 'NONE',  #8099 ) ;
#6524=ORIENTED_EDGE ( 'NONE', *, *, #14083, .T. ) ;
#6544=ORIENTED_EDGE ( 'NONE', *, *, #17260, .T. ) ;
#6566=DIRECTION ( 'NONE',  ( 0.000000000000000000, 0.000000000000000000, -1.000000000000000000 ) ) ;
#6603=VECTOR ( 'NONE', #11147, 1000.000000000000000 ) ;
#6628=VERTEX_POINT ( 'NONE', #13429 ) ;
#6651=ORIENTED_EDGE ( 'NONE', *, *, #7317, .F. ) ;
#6660=ORIENTED_EDGE ( 'NONE', *, *, #4043, .T. ) ;
#6686=ORIENTED_EDGE ( 'NONE', *, *, #13188, .T. ) ;
#6717=CARTESIAN_POINT ( 'NONE',  ( 5.000000000000000000, -4.685197434473809430, 6.071532165918824830E-15 ) ) ;
#6747=DIRECTION ( 'NONE',  ( 0.000000000000000000, -0.5000000000000013323, -0.8660254037844378194 ) ) ;
#6817=DIRECTION ( 'NONE',  ( 0.000000000000000000, 0.000000000000000000, 1.000000000000000000 ) ) ;
#6830=CARTESIAN_POINT ( 'NONE',  ( 0.000000000000000000, -2.342598717236899386, 4.057500000000001883 ) ) ;
#6885=ORIENTED_EDGE ( 'NONE', *, *, #15399, .T. ) ;
#6897=VECTOR ( 'NONE', #5434, 1000.000000000000000 ) ;
#6922=DIRECTION ( 'NONE',  ( 0.000000000000000000, 0.000000000000000000, 1.000000000000000000 ) ) ;
#6928=DIRECTION ( 'NONE',  ( 0.000000000000000000, -0.5000000000000013323, -0.8660254037844378194 ) ) ;
#6995=CARTESIAN_POINT ( 'NONE',  ( 5.000000000000000000, 7.027796151710712813, -4.057500000000007212 ) ) ;
#7014=ORIENTED_EDGE ( 'NONE', *, *, #12775, .T. ) ;
#7032=CARTESIAN_POINT ( 'NONE',  ( 5.000000000000000000, 3.513898075855357295, -2.028750000000006271 ) ) ;
#7037=FACE_OUTER_BOUND ( 'NONE', #9296, .T. ) ;
#7052=EDGE_LOOP ( 'NONE', ( #8810, #6524, #17718, #18197 ) ) ;
#7069=ORIENTED_EDGE ( 'NONE', *, *, #11206, .T. ) ;
#7089=FACE_OUTER_BOUND ( 'NONE', #7052, .T. ) ;
#7101=DIRECTION ( 'NONE',  ( -1.000000000000000000, -0.000000000000000000, -0.000000000000000000 ) ) ;
#7162=AXIS2_PLACEMENT_3D ( 'NONE', #6065, #7556, #12560 ) ;
#7182=CIRCLE ( 'NONE', #9875, 4.057500000000000107 ) ;
#7186=ORIENTED_EDGE ( 'NONE', *, *, #824, .F. ) ;
#7211=DIRECTION ( 'NONE',  ( 0.000000000000000000, 1.224646799147353207E-16, 1.000000000000000000 ) ) ;
#7247=EDGE_CURVE ( 'NONE', #4281, #456, #10269, .T. ) ;
#7259=FACE_OUTER_BOUND ( 'NONE', #1835, .T. ) ;
#7260=ORIENTED_EDGE ( 'NONE', *, *, #7708, .T. ) ;
#7263=CARTESIAN_POINT ( 'NONE',  ( 5.000000000000000000, 0.000000000000000000, 0.000000000000000000 ) ) ;
#7278=DIRECTION ( 'NONE',  ( -1.000000000000000000, -0.000000000000000000, -0.000000000000000000 ) ) ;
#7291=EDGE_CURVE ( 'NONE', #16434, #8493, #7723, .T. ) ;
#7296=CARTESIAN_POINT ( 'NONE',  ( -31.74999999999995737, 9.797174393178825657E-16, -8.000000000000000000 ) ) ;
#7317=EDGE_CURVE ( 'NONE', #279, #3078, #20659, .T. ) ;
#7363=CARTESIAN_POINT ( 'NONE',  ( 10.40000000000000036, 0.000000000000000000, 0.000000000000000000 ) ) ;
#7405=APPLICATION_CONTEXT ( 'automotive_design' ) ;
#7408=DIRECTION ( 'NONE',  ( 0.000000000000000000, 1.000000000000000000, -1.224646799147353207E-16 ) ) ;
#7409=CARTESIAN_POINT ( 'NONE',  ( 5.000000000000000000, 2.342598717236900718, -4.057500000000001883 ) ) ;
#7485=DIRECTION ( 'NONE',  ( -1.000000000000000000, -0.000000000000000000, -0.000000000000000000 ) ) ;
#7555=ORIENTED_EDGE ( 'NONE', *, *, #5788, .T. ) ;
#7556=DIRECTION ( 'NONE',  ( -0.000000000000000000, 0.8660254037844394848, 0.4999999999999985012 ) ) ;
#7587=CARTESIAN_POINT ( 'NONE',  ( 5.000000000000000000, 7.027796151710712813, -4.057500000000007212 ) ) ;
#7591=ADVANCED_FACE ( 'NONE', ( #4005 ), #522, .F. ) ;
#7617=DIRECTION ( 'NONE',  ( 0.000000000000000000, 0.000000000000000000, -1.000000000000000000 ) ) ;
#7667=VERTEX_POINT ( 'NONE', #18746 ) ;
#7708=EDGE_CURVE ( 'NONE', #8493, #18834, #6135, .T. ) ;
#7723=CIRCLE ( 'NONE', #8736, 0.4000000000000001887 ) ;
#7783=CARTESIAN_POINT ( 'NONE',  ( 5.000000000000000000, 7.027796151710712813, -4.057500000000007212 ) ) ;
#7793=CIRCLE ( 'NONE', #20657, 8.000000000000000000 ) ;
#7873=ORIENTED_EDGE ( 'NONE', *, *, #14321, .T. ) ;
#7897=VECTOR ( 'NONE', #17724, 999.9999999999998863 ) ;
#7925=CARTESIAN_POINT ( 'NONE',  ( 9.999999999999998224, 0.000000000000000000, -5.400000000000001243 ) ) ;
#7940=ORIENTED_EDGE ( 'NONE', *, *, #15347, .T. ) ;
#7947=CARTESIAN_POINT ( 'NONE',  ( 5.000000000000000000, 0.000000000000000000, 4.057500000000000107 ) ) ;
#7967=CARTESIAN_POINT ( 'NONE',  ( 10.40000000000000036, 0.000000000000000000, 0.000000000000000000 ) ) ;
#8006=DIRECTION ( 'NONE',  ( 0.000000000000000000, 0.000000000000000000, 1.000000000000000000 ) ) ;
#8039=ADVANCED_FACE ( 'NONE', ( #3245, #16495 ), #6516, .T. ) ;
#8051=EDGE_CURVE ( 'NONE', #10792, #18356, #390, .T. ) ;
#8099=AXIS2_PLACEMENT_3D ( 'NONE', #13113, #13014, #11411 ) ;
#8164=CARTESIAN_POINT ( 'NONE',  ( 1.500000000000001332, 0.000000000000000000, 0.000000000000000000 ) ) ;
#8338=EDGE_LOOP ( 'NONE', ( #19745, #15873 ) ) ;
#8381=CIRCLE ( 'NONE', #608, 5.000000000000000888 ) ;
#8398=SHAPE_REPRESENTATION ( 'socket head cap screw_iso_ISO 4762 M10 x 16 - 16N', ( #18233 ), #11452 ) ;
#8407=VECTOR ( 'NONE', #10613, 1000.000000000000000 ) ;
#8422=DIRECTION ( 'NONE',  ( -1.000000000000000000, -0.000000000000000000, -0.000000000000000000 ) ) ;
#8432=DIRECTION ( 'NONE',  ( 0.000000000000000000, 0.000000000000000000, 1.000000000000000000 ) ) ;
#8444=ORIENTED_EDGE ( 'NONE', *, *, #7317, .T. ) ;
#8493=VERTEX_POINT ( 'NONE', #18169 ) ;
#8498=DIRECTION ( 'NONE',  ( -0.5000000000000034417, 1.060575238724904696E-16, -0.8660254037844367092 ) ) ;
#8527=MECHANICAL_DESIGN_GEOMETRIC_PRESENTATION_REPRESENTATION('',(#9552),#13630);
#8552=PRODUCT ( 'socket head cap screw_iso_ISO 4762 M10 x 16 - 16N', 'socket head cap screw_iso_ISO 4762 M10 x 16 - 16N', '', ( #1188 ) ) ;
#8675=ORIENTED_EDGE ( 'NONE', *, *, #7247, .F. ) ;
#8678=VECTOR ( 'NONE', #10873, 1000.000000000000000 ) ;
#8681=VECTOR ( 'NONE', #11694, 1000.000000000000114 ) ;
#8694=ORIENTED_EDGE ( 'NONE', *, *, #17561, .F. ) ;
#8736=AXIS2_PLACEMENT_3D ( 'NONE', #11889, #7408, #7211 ) ;
#8759=EDGE_LOOP ( 'NONE', ( #16441, #8675, #6464, #19884, #17478 ) ) ;
#8780=ORIENTED_EDGE ( 'NONE', *, *, #1227, .F. ) ;
#8790=CARTESIAN_POINT ( 'NONE',  ( 0.000000000000000000, 0.000000000000000000, 0.000000000000000000 ) ) ;
#8810=ORIENTED_EDGE ( 'NONE', *, *, #13180, .T. ) ;
#8851=PLANE ( 'NONE',  #11164 ) ;
#8939=CARTESIAN_POINT ( 'NONE',  ( 1.500000000000001332, 7.960204194457796463E-16, -6.500000000000000888 ) ) ;
#8965=LINE ( 'NONE', #18416, #5275 ) ;
#8966=FACE_OUTER_BOUND ( 'NONE', #5640, .T. ) ;
#9074=CIRCLE ( 'NONE', #634, 8.000000000000000000 ) ;
#9086=ORIENTED_EDGE ( 'NONE', *, *, #19823, .F. ) ;
#9154=CARTESIAN_POINT ( 'NONE',  ( 1.500000000000001332, 0.000000000000000000, 0.000000000000000000 ) ) ;
#9195=ORIENTED_EDGE ( 'NONE', *, *, #4739, .F. ) ;
#9204=ORIENTED_EDGE ( 'NONE', *, *, #19625, .F. ) ;
#9241=AXIS2_PLACEMENT_3D ( 'NONE', #79, #8422, #13013 ) ;
#9257=VERTEX_POINT ( 'NONE', #15360 ) ;
#9296=EDGE_LOOP ( 'NONE', ( #10604, #5197, #7555, #9086 ) ) ;
#9302=FACE_OUTER_BOUND ( 'NONE', #15864, .T. ) ;
#9324=AXIS2_PLACEMENT_3D ( 'NONE', #12793, #19253, #11399 ) ;
#9381=( NAMED_UNIT ( * ) PLANE_ANGLE_UNIT ( ) SI_UNIT ( $, .RADIAN. ) );
#9411=DIRECTION ( 'NONE',  ( -1.000000000000000000, -0.000000000000000000, -0.000000000000000000 ) ) ;
#9427=ADVANCED_FACE ( 'NONE', ( #1336 ), #20508, .F. ) ;
#9437=LINE ( 'NONE', #1407, #6603 ) ;
#9446=DIRECTION ( 'NONE',  ( 0.000000000000000000, 0.000000000000000000, -1.000000000000000000 ) ) ;
#9530=ADVANCED_FACE ( 'NONE', ( #4819 ), #731, .F. ) ;
#9533=DIRECTION ( 'NONE',  ( 0.000000000000000000, 0.000000000000000000, 1.000000000000000000 ) ) ;
#9541=ORIENTED_EDGE ( 'NONE', *, *, #17600, .T. ) ;
#9552=STYLED_ITEM('',(#20995),#10492);
#9563=ORIENTED_EDGE ( 'NONE', *, *, #16779, .F. ) ;
#9612=LINE ( 'NONE', #1886, #11896 ) ;
#9618=DIRECTION ( 'NONE',  ( 0.000000000000000000, 0.4999999999999987232, -0.8660254037844393737 ) ) ;
#9713=DIRECTION ( 'NONE',  ( -1.000000000000000000, -0.000000000000000000, -0.000000000000000000 ) ) ;
#9721=CARTESIAN_POINT ( 'NONE',  ( 5.000000000000000000, -4.685197434473809430, 6.071532165918824830E-15 ) ) ;
#9733=ORIENTED_EDGE ( 'NONE', *, *, #1664, .F. ) ;
#9742=CARTESIAN_POINT ( 'NONE',  ( 26.00000000000000355, 5.109226446042757607E-16, -4.171999999999999709 ) ) ;
#9757=DIRECTION ( 'NONE',  ( -1.000000000000000000, -0.000000000000000000, -0.000000000000000000 ) ) ;
#9821=VECTOR ( 'NONE', #10254, 1000.000000000000000 ) ;
#9875=AXIS2_PLACEMENT_3D ( 'NONE', #7263, #18410, #8432 ) ;
#9907=VERTEX_POINT ( 'NONE', #13689 ) ;
#9939=LINE ( 'NONE', #6445, #20503 ) ;
#10049=AXIS2_PLACEMENT_3D ( 'NONE', #14080, #12694, #2935 ) ;
#10099=CARTESIAN_POINT ( 'NONE',  ( -31.74999999999995737, 0.000000000000000000, 0.000000000000000000 ) ) ;
#10183=DIRECTION ( 'NONE',  ( -1.000000000000000000, -0.000000000000000000, -0.000000000000000000 ) ) ;
#10194=DIRECTION ( 'NONE',  ( 1.000000000000000000, 0.000000000000000000, 0.000000000000000000 ) ) ;
#10209=( NAMED_UNIT ( * ) PLANE_ANGLE_UNIT ( ) SI_UNIT ( $, .RADIAN. ) );
#10210=DIRECTION ( 'NONE',  ( -1.000000000000000000, -0.000000000000000000, -0.000000000000000000 ) ) ;
#10214=ORIENTED_EDGE ( 'NONE', *, *, #3697, .T. ) ;
#10254=DIRECTION ( 'NONE',  ( -0.7071067811865331398, 0.000000000000000000, 0.7071067811865620056 ) ) ;
#10258=ORIENTED_EDGE ( 'NONE', *, *, #5788, .F. ) ;
#10269=LINE ( 'NONE', #3820, #5006 ) ;
#10276=FACE_OUTER_BOUND ( 'NONE', #4778, .T. ) ;
#10283=DIRECTION ( 'NONE',  ( 0.000000000000000000, 0.000000000000000000, 1.000000000000000000 ) ) ;
#10342=AXIS2_PLACEMENT_3D ( 'NONE', #7587, #10764, #12481 ) ;
#10350=ORIENTED_EDGE ( 'NONE', *, *, #20306, .F. ) ;
#10352=LINE ( 'NONE', #523, #2926 ) ;
#10354=AXIS2_PLACEMENT_3D ( 'NONE', #16563, #2045, #10283 ) ;
#10411=VERTEX_POINT ( 'NONE', #519 ) ;
#10461=ORIENTED_EDGE ( 'NONE', *, *, #20287, .T. ) ;
#10462=ORIENTED_EDGE ( 'NONE', *, *, #2540, .T. ) ;
#10473=FACE_OUTER_BOUND ( 'NONE', #3337, .T. ) ;
#10474=EDGE_LOOP ( 'NONE', ( #10258, #7069, #525, #19855 ) ) ;
#10484=DIRECTION ( 'NONE',  ( 1.000000000000000000, 0.000000000000000000, 0.000000000000000000 ) ) ;
#10492=MANIFOLD_SOLID_BREP ( 'Hex', #20828 ) ;
#10531=LINE ( 'NONE', #3971, #12675 ) ;
#10543=AXIS2_PLACEMENT_3D ( 'NONE', #12353, #17010, #14161 ) ;
#10604=ORIENTED_EDGE ( 'NONE', *, *, #18111, .T. ) ;
#10613=DIRECTION ( 'NONE',  ( -1.000000000000000000, -0.000000000000000000, -0.000000000000000000 ) ) ;
#10645=ORIENTED_EDGE ( 'NONE', *, *, #2540, .F. ) ;
#10661=EDGE_CURVE ( 'NONE', #15787, #9257, #172, .T. ) ;
#10686=CIRCLE ( 'NONE', #17488, 5.000000000000000888 ) ;
#10729=VECTOR ( 'NONE', #19917, 1000.000000000000000 ) ;
#10746=AXIS2_PLACEMENT_3D ( 'NONE', #16468, #3330, #11702 ) ;
#10750=DIRECTION ( 'NONE',  ( -1.000000000000000000, -0.000000000000000000, -0.000000000000000000 ) ) ;
#10764=DIRECTION ( 'NONE',  ( 1.000000000000000000, 0.000000000000000000, 0.000000000000000000 ) ) ;
#10779=VERTEX_POINT ( 'NONE', #20104 ) ;
#10792=VERTEX_POINT ( 'NONE', #11955 ) ;
#10794=LINE ( 'NONE', #14219, #17527 ) ;
#10838=ORIENTED_EDGE ( 'NONE', *, *, #13188, .F. ) ;
#10844=EDGE_CURVE ( 'NONE', #20933, #4158, #17029, .T. ) ;
#10860=AXIS2_PLACEMENT_3D ( 'NONE', #13026, #9713, #6422 ) ;
#10873=DIRECTION ( 'NONE',  ( -1.000000000000000000, -0.000000000000000000, -0.000000000000000000 ) ) ;
#10903=AXIS2_PLACEMENT_3D ( 'NONE', #17230, #10750, #13959 ) ;
#10950=DIRECTION ( 'NONE',  ( -1.000000000000000000, -0.000000000000000000, -0.000000000000000000 ) ) ;
#11016=PLANE ( 'NONE',  #11758 ) ;
#11033=VERTEX_POINT ( 'NONE', #13626 ) ;
#11100=DIRECTION ( 'NONE',  ( -1.000000000000000000, -0.000000000000000000, -0.000000000000000000 ) ) ;
#11118=FACE_OUTER_BOUND ( 'NONE', #11516, .T. ) ;
#11126=EDGE_LOOP ( 'NONE', ( #12384, #7260 ) ) ;
#11147=DIRECTION ( 'NONE',  ( -1.000000000000000000, -0.000000000000000000, -0.000000000000000000 ) ) ;
#11161=ORIENTED_EDGE ( 'NONE', *, *, #14196, .F. ) ;
#11164=AXIS2_PLACEMENT_3D ( 'NONE', #4194, #15353, #807 ) ;
#11196=ORIENTED_EDGE ( 'NONE', *, *, #3382, .T. ) ;
#11206=EDGE_CURVE ( 'NONE', #1032, #6628, #13949, .T. ) ;
#11226=ADVANCED_FACE ( 'NONE', ( #20281 ), #5743, .T. ) ;
#11267=CARTESIAN_POINT ( 'NONE',  ( 10.40000000000000036, 0.000000000000000000, 0.000000000000000000 ) ) ;
#11294=ORIENTED_EDGE ( 'NONE', *, *, #14321, .F. ) ;
#11380=CIRCLE ( 'NONE', #1232, 4.057500000000000107 ) ;
#11399=DIRECTION ( 'NONE',  ( 0.000000000000000000, -1.000000000000000000, 1.295896757998782163E-15 ) ) ;
#11410=DIRECTION ( 'NONE',  ( 0.000000000000000000, -0.4999999999999987232, 0.8660254037844393737 ) ) ;
#11411=DIRECTION ( 'NONE',  ( 0.000000000000000000, 0.000000000000000000, -1.000000000000000000 ) ) ;
#11419=AXIS2_PLACEMENT_3D ( 'NONE', #8790, #15593, #15495 ) ;
#11427=AXIS2_PLACEMENT_3D ( 'NONE', #14429, #11435, #4558 ) ;
#11435=DIRECTION ( 'NONE',  ( -1.000000000000000000, -0.000000000000000000, -0.000000000000000000 ) ) ;
#11451=VECTOR ( 'NONE', #4460, 1000.000000000000000 ) ;
#11452=( GEOMETRIC_REPRESENTATION_CONTEXT ( 3 ) GLOBAL_UNCERTAINTY_ASSIGNED_CONTEXT ( ( #13836 ) ) GLOBAL_UNIT_ASSIGNED_CONTEXT ( ( #488, #10209, #19967 ) ) REPRESENTATION_CONTEXT ( 'NONE', 'WORKASPACE' ) );
#11462=FACE_OUTER_BOUND ( 'NONE', #98, .T. ) ;
#11472=ORIENTED_EDGE ( 'NONE', *, *, #8051, .F. ) ;
#11494=VERTEX_POINT ( 'NONE', #13025 ) ;
#11516=EDGE_LOOP ( 'NONE', ( #18851, #20805 ) ) ;
#11517=ORIENTED_EDGE ( 'NONE', *, *, #3280, .F. ) ;
#11553=ORIENTED_EDGE ( 'NONE', *, *, #14961, .T. ) ;
#11600=ORIENTED_EDGE ( 'NONE', *, *, #13180, .F. ) ;
#11688=ORIENTED_EDGE ( 'NONE', *, *, #824, .T. ) ;
#11694=DIRECTION ( 'NONE',  ( 0.000000000000000000, 0.4999999999999985012, -0.8660254037844394848 ) ) ;
#11702=DIRECTION ( 'NONE',  ( 0.000000000000000000, 0.000000000000000000, -1.000000000000000000 ) ) ;
#11718=LINE ( 'NONE', #4073, #6897 ) ;
#11758=AXIS2_PLACEMENT_3D ( 'NONE', #12716, #20648, #9618 ) ;
#11772=ORIENTED_EDGE ( 'NONE', *, *, #2403, .T. ) ;
#11776=CIRCLE ( 'NONE', #11427, 6.500000000000000888 ) ;
#11811=ORIENTED_EDGE ( 'NONE', *, *, #2403, .F. ) ;
#11888=CIRCLE ( 'NONE', #10860, 8.000000000000000000 ) ;
#11889=CARTESIAN_POINT ( 'NONE',  ( 10.40000000000000036, 6.613092715395708453E-16, 5.400000000000001243 ) ) ;
#11893=CARTESIAN_POINT ( 'NONE',  ( 0.000000000000000000, 0.000000000000000000, 6.500000000000000888 ) ) ;
#11896=VECTOR ( 'NONE', #19465, 1000.000000000000000 ) ;
#11955=CARTESIAN_POINT ( 'NONE',  ( 5.000000000000000000, 2.342598717236900718, -4.057500000000001883 ) ) ;
#11981=CARTESIAN_POINT ( 'NONE',  ( -31.74999999999995737, 0.000000000000000000, 0.000000000000000000 ) ) ;
#11999=EDGE_LOOP ( 'NONE', ( #8444, #3771, #11517 ) ) ;
#12144=ORIENTED_EDGE ( 'NONE', *, *, #17600, .F. ) ;
#12156=ORIENTED_EDGE ( 'NONE', *, *, #8051, .T. ) ;
#12175=ORIENTED_EDGE ( 'NONE', *, *, #20287, .F. ) ;
#12200=CIRCLE ( 'NONE', #18, 4.171999999999999709 ) ;
#12205=DIRECTION ( 'NONE',  ( 0.000000000000000000, 0.000000000000000000, -1.000000000000000000 ) ) ;
#12247=TOROIDAL_SURFACE ( 'NONE', #5789, 6.500000000000000888, 1.500000000000000000 ) ;
#12263=CARTESIAN_POINT ( 'NONE',  ( 5.000000000000000000, 0.000000000000000000, 0.000000000000000000 ) ) ;
#12290=DIRECTION ( 'NONE',  ( -1.000000000000000000, -0.000000000000000000, -0.000000000000000000 ) ) ;
#12327=DIRECTION ( 'NONE',  ( 0.000000000000000000, 0.8660254037844379305, -0.5000000000000014433 ) ) ;
#12353=CARTESIAN_POINT ( 'NONE',  ( 5.000000000000000000, 0.000000000000000000, 0.000000000000000000 ) ) ;
#12357=DIRECTION ( 'NONE',  ( 0.000000000000000000, -0.5000000000000009992, -0.8660254037844380415 ) ) ;
#12376=DIRECTION ( 'NONE',  ( 0.000000000000000000, -1.000000000000000000, 0.000000000000000000 ) ) ;
#12384=ORIENTED_EDGE ( 'NONE', *, *, #20306, .T. ) ;
#12420=CARTESIAN_POINT ( 'NONE',  ( -31.74999999999995737, 0.000000000000000000, 8.000000000000000000 ) ) ;
#12481=DIRECTION ( 'NONE',  ( 0.000000000000000000, 0.000000000000000000, -1.000000000000000000 ) ) ;
#12520=LINE ( 'NONE', #7409, #4866 ) ;
#12560=DIRECTION ( 'NONE',  ( 0.000000000000000000, -0.4999999999999985012, 0.8660254037844394848 ) ) ;
#12588=AXIS2_PLACEMENT_3D ( 'NONE', #9154, #4510, #14060 ) ;
#12616=DIRECTION ( 'NONE',  ( 0.000000000000000000, -0.5000000000000009992, -0.8660254037844380415 ) ) ;
#12617=CARTESIAN_POINT ( 'NONE',  ( 1.500000000000001332, 0.000000000000000000, 8.000000000000000000 ) ) ;
#12673=ORIENTED_EDGE ( 'NONE', *, *, #20015, .T. ) ;
#12675=VECTOR ( 'NONE', #6928, 1000.000000000000114 ) ;
#12685=DIRECTION ( 'NONE',  ( 0.000000000000000000, 0.000000000000000000, -1.000000000000000000 ) ) ;
#12694=DIRECTION ( 'NONE',  ( -1.000000000000000000, -0.000000000000000000, -0.000000000000000000 ) ) ;
#12703=EDGE_LOOP ( 'NONE', ( #9195, #13238, #10350, #13200 ) ) ;
#12716=CARTESIAN_POINT ( 'NONE',  ( 5.000000000000000000, 4.685197434473812983, -6.938893903907228378E-15 ) ) ;
#12717=AXIS2_PLACEMENT_3D ( 'NONE', #5833, #4037, #17092 ) ;
#12770=DIRECTION ( 'NONE',  ( 0.000000000000000000, 0.000000000000000000, -1.000000000000000000 ) ) ;
#12775=EDGE_CURVE ( 'NONE', #10411, #3183, #19796, .T. ) ;
#12793=CARTESIAN_POINT ( 'NONE',  ( 5.000000000000000000, -2.342598717236899386, 4.057500000000001883 ) ) ;
#13013=DIRECTION ( 'NONE',  ( 0.000000000000000000, 0.000000000000000000, 1.000000000000000000 ) ) ;
#13014=DIRECTION ( 'NONE',  ( 1.000000000000000000, 0.000000000000000000, 0.000000000000000000 ) ) ;
#13025=CARTESIAN_POINT ( 'NONE',  ( 0.000000000000000000, -4.685197434473809430, 6.071532165918824830E-15 ) ) ;
#13026=CARTESIAN_POINT ( 'NONE',  ( 10.00000000000000178, 0.000000000000000000, 0.000000000000000000 ) ) ;
#13068=ORIENTED_EDGE ( 'NONE', *, *, #1389, .T. ) ;
#13070=ADVANCED_FACE ( 'NONE', ( #15993, #1251 ), #1458, .T. ) ;
#13110=DIRECTION ( 'NONE',  ( 0.000000000000000000, 0.4999999999999985012, -0.8660254037844394848 ) ) ;
#13113=CARTESIAN_POINT ( 'NONE',  ( 9.999999999999998224, 8.000000000000000000, 0.000000000000000000 ) ) ;
#13180=EDGE_CURVE ( 'NONE', #16971, #14800, #17391, .T. ) ;
#13188=EDGE_CURVE ( 'NONE', #10411, #16948, #16293, .T. ) ;
#13200=ORIENTED_EDGE ( 'NONE', *, *, #1389, .F. ) ;
#13238=ORIENTED_EDGE ( 'NONE', *, *, #7291, .T. ) ;
#13301=DIRECTION ( 'NONE',  ( 0.000000000000000000, 0.000000000000000000, 1.000000000000000000 ) ) ;
#13429=CARTESIAN_POINT ( 'NONE',  ( 0.000000000000000000, 8.878689293818310074E-16, -6.500000000000000888 ) ) ;
#13438=ADVANCED_FACE ( 'NONE', ( #11462 ), #20419, .F. ) ;
#13455=DIRECTION ( 'NONE',  ( 0.000000000000000000, 0.000000000000000000, -1.000000000000000000 ) ) ;
#13470=VERTEX_POINT ( 'NONE', #14675 ) ;
#13525=APPLICATION_CONTEXT ( 'automotive_design' ) ;
#13536=ORIENTED_EDGE ( 'NONE', *, *, #3382, .F. ) ;
#13626=CARTESIAN_POINT ( 'NONE',  ( 0.000000000000000000, 2.342598717236900718, -4.057500000000001883 ) ) ;
#13630=( GEOMETRIC_REPRESENTATION_CONTEXT ( 3 ) GLOBAL_UNCERTAINTY_ASSIGNED_CONTEXT ( ( #1730 ) ) GLOBAL_UNIT_ASSIGNED_CONTEXT ( ( #2942, #9381, #1351 ) ) REPRESENTATION_CONTEXT ( 'NONE', 'WORKASPACE' ) );
#13666=DIRECTION ( 'NONE',  ( 1.000000000000000000, 0.000000000000000000, 0.000000000000000000 ) ) ;
#13689=CARTESIAN_POINT ( 'NONE',  ( 26.00000000000000355, 5.616230220889761452E-16, -4.171999999999999709 ) ) ;
#13749=FACE_OUTER_BOUND ( 'NONE', #12703, .T. ) ;
#13767=DIRECTION ( 'NONE',  ( 0.000000000000000000, 0.000000000000000000, -1.000000000000000000 ) ) ;
#13787=CARTESIAN_POINT ( 'NONE',  ( -31.74999999999995737, 0.000000000000000000, 0.000000000000000000 ) ) ;
#13801=EDGE_CURVE ( 'NONE', #10792, #11033, #12520, .T. ) ;
#13836=UNCERTAINTY_MEASURE_WITH_UNIT (LENGTH_MEASURE( 1.000000000000000082E-05 ), #488, 'distance_accuracy_value', 'NONE');
#13863=FACE_OUTER_BOUND ( 'NONE', #20545, .T. ) ;
#13899=DIRECTION ( 'NONE',  ( -1.000000000000000000, -0.000000000000000000, -0.000000000000000000 ) ) ;
#13949=CIRCLE ( 'NONE', #1083, 1.499999999999999556 ) ;
#13959=DIRECTION ( 'NONE',  ( 0.000000000000000000, 0.000000000000000000, 1.000000000000000000 ) ) ;
#13962=DIRECTION ( 'NONE',  ( -1.000000000000000000, -0.000000000000000000, -0.000000000000000000 ) ) ;
#13978=DIRECTION ( 'NONE',  ( 0.000000000000000000, 0.000000000000000000, 1.000000000000000000 ) ) ;
#14006=PRODUCT_DEFINITION_SHAPE ( 'NONE', 'NONE',  #16891 ) ;
#14060=DIRECTION ( 'NONE',  ( 0.000000000000000000, 0.000000000000000000, 1.000000000000000000 ) ) ;
#14080=CARTESIAN_POINT ( 'NONE',  ( 26.00000000000000355, 0.000000000000000000, 0.000000000000000000 ) ) ;
#14083=EDGE_CURVE ( 'NONE', #14800, #2300, #10352, .T. ) ;
#14134=DIRECTION ( 'NONE',  ( -1.000000000000000000, -0.000000000000000000, -0.000000000000000000 ) ) ;
#14138=CARTESIAN_POINT ( 'NONE',  ( 1.500000000000001332, 9.797174393178825657E-16, -8.000000000000000000 ) ) ;
#14161=DIRECTION ( 'NONE',  ( 0.000000000000000000, 0.000000000000000000, 1.000000000000000000 ) ) ;
#14196=EDGE_CURVE ( 'NONE', #14800, #16971, #10686, .T. ) ;
#14219=CARTESIAN_POINT ( 'NONE',  ( 5.000000000000000000, -2.342598717236899386, 4.057500000000001883 ) ) ;
#14248=CARTESIAN_POINT ( 'NONE',  ( 0.000000000000000000, 4.685197434473812983, -6.938893903907228378E-15 ) ) ;
#14267=EDGE_LOOP ( 'NONE', ( #10461, #14841, #4365 ) ) ;
#14269=DIRECTION ( 'NONE',  ( -0.000000000000000000, 1.000000000000000000, 1.224646799147353207E-16 ) ) ;
#14288=DIRECTION ( 'NONE',  ( 1.000000000000000000, 0.000000000000000000, 0.000000000000000000 ) ) ;
#14321=EDGE_CURVE ( 'NONE', #16948, #3183, #11380, .T. ) ;
#14364=VERTEX_POINT ( 'NONE', #16496 ) ;
#14426=CONICAL_SURFACE ( 'NONE', #2895, 4.171999999999999709, 0.7853981633974687071 ) ;
#14429=CARTESIAN_POINT ( 'NONE',  ( 0.000000000000000000, 0.000000000000000000, 0.000000000000000000 ) ) ;
#14432=CARTESIAN_POINT ( 'NONE',  ( 5.000000000000000000, -2.342598717236899386, 4.057500000000001883 ) ) ;
#14498=PLANE ( 'NONE',  #9324 ) ;
#14515=EDGE_LOOP ( 'NONE', ( #9541, #9204, #12175, #11472, #15671 ) ) ;
#14556=CARTESIAN_POINT ( 'NONE',  ( 5.000000000000000000, -4.506943796211480446E-15, -4.057500000000000107 ) ) ;
#14577=ADVANCED_FACE ( 'NONE', ( #7259 ), #2210, .F. ) ;
#14581=CARTESIAN_POINT ( 'NONE',  ( 0.000000000000000000, 2.342598717236900718, -4.057500000000001883 ) ) ;
#14674=AXIS2_PLACEMENT_3D ( 'NONE', #6196, #12376, #18835 ) ;
#14675=CARTESIAN_POINT ( 'NONE',  ( 10.00000000000000178, 9.797174393178825657E-16, -8.000000000000000000 ) ) ;
#14676=DIRECTION ( 'NONE',  ( -1.000000000000000000, -0.000000000000000000, -0.000000000000000000 ) ) ;
#14721=EDGE_CURVE ( 'NONE', #11494, #2878, #1841, .T. ) ;
#14800=VERTEX_POINT ( 'NONE', #20470 ) ;
#14804=ORIENTED_EDGE ( 'NONE', *, *, #1207, .T. ) ;
#14841=ORIENTED_EDGE ( 'NONE', *, *, #18769, .F. ) ;
#14861=DIRECTION ( 'NONE',  ( 0.000000000000000000, -0.5000000000000013323, -0.8660254037844378194 ) ) ;
#14901=DIRECTION ( 'NONE',  ( 1.000000000000000000, 0.000000000000000000, 0.000000000000000000 ) ) ;
#14961=EDGE_CURVE ( 'NONE', #456, #11494, #19107, .T. ) ;
#14990=LINE ( 'NONE', #16553, #1724 ) ;
#15020=VECTOR ( 'NONE', #6747, 1000.000000000000114 ) ;
#15044=EDGE_LOOP ( 'NONE', ( #8780, #11688, #3687, #1953, #11196 ) ) ;
#15064=AXIS2_PLACEMENT_3D ( 'NONE', #13787, #20235, #1065 ) ;
#15123=AXIS2_PLACEMENT_3D ( 'NONE', #11981, #530, #18440 ) ;
#15128=ADVANCED_FACE ( 'NONE', ( #9302 ), #14426, .T. ) ;
#15185=CIRCLE ( 'NONE', #20893, 4.057500000000000107 ) ;
#15202=FACE_OUTER_BOUND ( 'NONE', #14515, .T. ) ;
#15216=ADVANCED_FACE ( 'NONE', ( #15202 ), #16766, .F. ) ;
#15307=AXIS2_PLACEMENT_3D ( 'NONE', #17041, #2519, #20311 ) ;
#15347=EDGE_CURVE ( 'NONE', #3183, #18356, #1230, .T. ) ;
#15353=DIRECTION ( 'NONE',  ( 1.000000000000000000, 0.000000000000000000, 0.000000000000000000 ) ) ;
#15360=CARTESIAN_POINT ( 'NONE',  ( 5.000000000000000000, -3.513898075855360847, -2.028749999999992504 ) ) ;
#15383=VECTOR ( 'NONE', #121, 1000.000000000000000 ) ;
#15399=EDGE_CURVE ( 'NONE', #3183, #10792, #9939, .T. ) ;
#15411=PLANE ( 'NONE',  #1711 ) ;
#15454=DIRECTION ( 'NONE',  ( 0.000000000000000000, 0.000000000000000000, 1.000000000000000000 ) ) ;
#15466=DIRECTION ( 'NONE',  ( 0.000000000000000000, 1.000000000000000000, -1.295896757998782163E-15 ) ) ;
#15495=DIRECTION ( 'NONE',  ( 0.000000000000000000, 0.000000000000000000, 1.000000000000000000 ) ) ;
#15498=DIRECTION ( 'NONE',  ( 0.000000000000000000, 0.000000000000000000, -1.000000000000000000 ) ) ;
#15548=ADVANCED_FACE ( 'NONE', ( #7089 ), #5379, .T. ) ;
#15562=ORIENTED_EDGE ( 'NONE', *, *, #19625, .T. ) ;
#15577=AXIS2_PLACEMENT_3D ( 'NONE', #7363, #20894, #9446 ) ;
#15593=DIRECTION ( 'NONE',  ( -1.000000000000000000, -0.000000000000000000, -0.000000000000000000 ) ) ;
#15596=DIRECTION ( 'NONE',  ( 0.000000000000000000, -1.000000000000000000, 0.000000000000000000 ) ) ;
#15637=AXIS2_PLACEMENT_3D ( 'NONE', #8164, #14676, #16444 ) ;
#15638=DIRECTION ( 'NONE',  ( 0.000000000000000000, 0.000000000000000000, 1.000000000000000000 ) ) ;
#15643=ORIENTED_EDGE ( 'NONE', *, *, #19823, .T. ) ;
#15671=ORIENTED_EDGE ( 'NONE', *, *, #13801, .T. ) ;
#15706=CARTESIAN_POINT ( 'NONE',  ( 10.40000000000000036, 0.000000000000000000, -5.400000000000001243 ) ) ;
#15772=CARTESIAN_POINT ( 'NONE',  ( -31.74999999999995737, 0.000000000000000000, 5.000000000000000888 ) ) ;
#15787=VERTEX_POINT ( 'NONE', #190 ) ;
#15842=VECTOR ( 'NONE', #4708, 1000.000000000000000 ) ;
#15857=PLANE ( 'NONE',  #19891 ) ;
#15864=EDGE_LOOP ( 'NONE', ( #6544, #14804, #11600, #20130 ) ) ;
#15873=ORIENTED_EDGE ( 'NONE', *, *, #5629, .F. ) ;
#15882=PRODUCT_DEFINITION_FORMATION_WITH_SPECIFIED_SOURCE ( 'ANY', '', #8552, .NOT_KNOWN. ) ;
#15903=CARTESIAN_POINT ( 'NONE',  ( 0.000000000000000000, 0.000000000000000000, 0.000000000000000000 ) ) ;
#15962=EDGE_CURVE ( 'NONE', #4281, #279, #8965, .T. ) ;
#15967=ORIENTED_EDGE ( 'NONE', *, *, #1207, .F. ) ;
#15972=ORIENTED_EDGE ( 'NONE', *, *, #16041, .T. ) ;
#15993=FACE_BOUND ( 'NONE', #5600, .T. ) ;
#16041=EDGE_CURVE ( 'NONE', #16971, #16434, #1239, .T. ) ;
#16132=LINE ( 'NONE', #529, #9821 ) ;
#16141=LINE ( 'NONE', #4782, #19335 ) ;
#16177=DIRECTION ( 'NONE',  ( -1.000000000000000000, -0.000000000000000000, -0.000000000000000000 ) ) ;
#16293=LINE ( 'NONE', #3350, #16707 ) ;
#16380=ORIENTED_EDGE ( 'NONE', *, *, #17445, .F. ) ;
#16434=VERTEX_POINT ( 'NONE', #6348 ) ;
#16436=ORIENTED_EDGE ( 'NONE', *, *, #18769, .T. ) ;
#16441=ORIENTED_EDGE ( 'NONE', *, *, #14961, .F. ) ;
#16444=DIRECTION ( 'NONE',  ( 0.000000000000000000, 0.000000000000000000, 1.000000000000000000 ) ) ;
#16458=CARTESIAN_POINT ( 'NONE',  ( 10.40000000000000036, 0.000000000000000000, 0.000000000000000000 ) ) ;
#16468=CARTESIAN_POINT ( 'NONE',  ( 9.999999999999998224, 0.000000000000000000, 0.000000000000000000 ) ) ;
#16495=FACE_OUTER_BOUND ( 'NONE', #8338, .T. ) ;
#16496=CARTESIAN_POINT ( 'NONE',  ( 7.342598717236928252, 0.000000000000000000, 0.000000000000000000 ) ) ;
#16513=CIRCLE ( 'NONE', #10746, 5.400000000000001243 ) ;
#16515=CARTESIAN_POINT ( 'NONE',  ( 25.17200000000003612, 0.000000000000000000, 5.000000000000000888 ) ) ;
#16553=CARTESIAN_POINT ( 'NONE',  ( 5.000000000000000000, 4.685197434473812983, -6.938893903907228378E-15 ) ) ;
#16563=CARTESIAN_POINT ( 'NONE',  ( 26.00000000000000355, 0.000000000000000000, 0.000000000000000000 ) ) ;
#16574=CARTESIAN_POINT ( 'NONE',  ( 5.000000000000000000, 7.027796151710712813, -4.057500000000007212 ) ) ;
#16608=ORIENTED_EDGE ( 'NONE', *, *, #3697, .F. ) ;
#16643=EDGE_LOOP ( 'NONE', ( #12673, #2186 ) ) ;
#16660=FACE_OUTER_BOUND ( 'NONE', #17037, .T. ) ;
#16661=ORIENTED_EDGE ( 'NONE', *, *, #12775, .F. ) ;
#16672=VERTEX_POINT ( 'NONE', #19705 ) ;
#16687=EDGE_CURVE ( 'NONE', #6628, #4158, #18873, .T. ) ;
#16707=VECTOR ( 'NONE', #11410, 1000.000000000000000 ) ;
#16766=PLANE ( 'NONE',  #12717 ) ;
#16779=EDGE_CURVE ( 'NONE', #13470, #1032, #5593, .T. ) ;
#16876=EDGE_CURVE ( 'NONE', #4281, #7667, #10794, .T. ) ;
#16891=PRODUCT_DEFINITION ( 'UNKNOWN', '', #15882, #1319 ) ;
#16895=ORIENTED_EDGE ( 'NONE', *, *, #10661, .F. ) ;
#16904=ADVANCED_FACE ( 'NONE', ( #2862 ), #11016, .T. ) ;
#16905=ORIENTED_EDGE ( 'NONE', *, *, #11206, .F. ) ;
#16909=ADVANCED_FACE ( 'NONE', ( #11118 ), #17272, .T. ) ;
#16948=VERTEX_POINT ( 'NONE', #3167 ) ;
#16971=VERTEX_POINT ( 'NONE', #16515 ) ;
#16988=LINE ( 'NONE', #2469, #8407 ) ;
#16990=CARTESIAN_POINT ( 'NONE',  ( 10.40000000000000036, 6.123233995736767268E-16, -5.000000000000000888 ) ) ;
#16999=ORIENTED_EDGE ( 'NONE', *, *, #2100, .F. ) ;
#17010=DIRECTION ( 'NONE',  ( -1.000000000000000000, -0.000000000000000000, -0.000000000000000000 ) ) ;
#17029=CIRCLE ( 'NONE', #14674, 1.499999999999999556 ) ;
#17037=EDGE_LOOP ( 'NONE', ( #3191, #3875, #13536 ) ) ;
#17041=CARTESIAN_POINT ( 'NONE',  ( -31.74999999999995737, 0.000000000000000000, 0.000000000000000000 ) ) ;
#17046=AXIS2_PLACEMENT_3D ( 'NONE', #4531, #17679, #1663 ) ;
#17092=DIRECTION ( 'NONE',  ( 0.000000000000000000, 1.000000000000000000, -1.110768649713242108E-15 ) ) ;
#17230=CARTESIAN_POINT ( 'NONE',  ( 5.000000000000000000, 0.000000000000000000, 0.000000000000000000 ) ) ;
#17260=EDGE_CURVE ( 'NONE', #19392, #9907, #4325, .T. ) ;
#17263=ORIENTED_EDGE ( 'NONE', *, *, #7708, .F. ) ;
#17272=PLANE ( 'NONE',  #19201 ) ;
#17279=DIRECTION ( 'NONE',  ( -1.000000000000000000, -0.000000000000000000, -0.000000000000000000 ) ) ;
#17308=EDGE_CURVE ( 'NONE', #18356, #9257, #15185, .T. ) ;
#17391=CIRCLE ( 'NONE', #9241, 5.000000000000000888 ) ;
#17445=EDGE_CURVE ( 'NONE', #7667, #15787, #20709, .T. ) ;
#17478=ORIENTED_EDGE ( 'NONE', *, *, #18305, .T. ) ;
#17488=AXIS2_PLACEMENT_3D ( 'NONE', #935, #7278, #2845 ) ;
#17518=CARTESIAN_POINT ( 'NONE',  ( 26.00000000000000355, 0.000000000000000000, 4.171999999999999709 ) ) ;
#17527=VECTOR ( 'NONE', #12616, 1000.000000000000114 ) ;
#17541=VECTOR ( 'NONE', #12357, 1000.000000000000114 ) ;
#17561=EDGE_CURVE ( 'NONE', #2300, #16434, #8381, .T. ) ;
#17600=EDGE_CURVE ( 'NONE', #11033, #2878, #1629, .T. ) ;
#17620=CARTESIAN_POINT ( 'NONE',  ( 0.000000000000000000, -2.342598717236899386, 4.057500000000001883 ) ) ;
#17653=TOROIDAL_SURFACE ( 'NONE', #15637, 6.500000000000000888, 1.500000000000000000 ) ;
#17679=DIRECTION ( 'NONE',  ( -1.000000000000000000, 0.000000000000000000, -0.000000000000000000 ) ) ;
#17718=ORIENTED_EDGE ( 'NONE', *, *, #17561, .T. ) ;
#17724=DIRECTION ( 'NONE',  ( -0.5000000000000034417, 0.000000000000000000, 0.8660254037844367092 ) ) ;
#17928=EDGE_LOOP ( 'NONE', ( #15967, #3082, #239, #11161 ) ) ;
#18064=PLANE ( 'NONE',  #19223 ) ;
#18094=ORIENTED_EDGE ( 'NONE', *, *, #13801, .F. ) ;
#18111=EDGE_CURVE ( 'NONE', #18707, #13470, #9074, .T. ) ;
#18140=ORIENTED_EDGE ( 'NONE', *, *, #4597, .F. ) ;
#18154=CARTESIAN_POINT ( 'NONE',  ( 5.000000000000000000, 4.969004387540385421E-16, -4.057500000000000107 ) ) ;
#18169=CARTESIAN_POINT ( 'NONE',  ( 9.999999999999998224, 6.613092715395708453E-16, 5.400000000000001243 ) ) ;
#18195=EDGE_LOOP ( 'NONE', ( #6885, #12156, #5177 ) ) ;
#18197=ORIENTED_EDGE ( 'NONE', *, *, #16041, .F. ) ;
#18233=AXIS2_PLACEMENT_3D ( 'NONE', #15903, #1274, #19656 ) ;
#18303=VERTEX_POINT ( 'NONE', #14248 ) ;
#18305=EDGE_CURVE ( 'NONE', #15787, #11494, #16988, .T. ) ;
#18356=VERTEX_POINT ( 'NONE', #14556 ) ;
#18410=DIRECTION ( 'NONE',  ( -1.000000000000000000, -0.000000000000000000, -0.000000000000000000 ) ) ;
#18416=CARTESIAN_POINT ( 'NONE',  ( 5.000000000000000000, -2.342598717236899386, 4.057500000000001883 ) ) ;
#18440=DIRECTION ( 'NONE',  ( 0.000000000000000000, 0.000000000000000000, 1.000000000000000000 ) ) ;
#18507=ORIENTED_EDGE ( 'NONE', *, *, #4043, .F. ) ;
#18671=ORIENTED_EDGE ( 'NONE', *, *, #5629, .T. ) ;
#18703=EDGE_LOOP ( 'NONE', ( #11811, #18507, #6686, #20121, #2012 ) ) ;
#18707=VERTEX_POINT ( 'NONE', #1066 ) ;
#18739=EDGE_LOOP ( 'NONE', ( #16895, #16380, #18140 ) ) ;
#18746=CARTESIAN_POINT ( 'NONE',  ( 5.000000000000000000, -3.513898075855355074, 2.028750000000002274 ) ) ;
#18769=EDGE_CURVE ( 'NONE', #9257, #16672, #1277, .T. ) ;
#18834=VERTEX_POINT ( 'NONE', #7925 ) ;
#18835=DIRECTION ( 'NONE',  ( 0.000000000000000000, 0.000000000000000000, -1.000000000000000000 ) ) ;
#18851=ORIENTED_EDGE ( 'NONE', *, *, #17260, .F. ) ;
#18873=CIRCLE ( 'NONE', #11419, 6.500000000000000888 ) ;
#19107=LINE ( 'NONE', #17620, #1216 ) ;
#19134=DIRECTION ( 'NONE',  ( 0.000000000000000000, 0.8660254037844380415, -0.5000000000000009992 ) ) ;
#19201=AXIS2_PLACEMENT_3D ( 'NONE', #3064, #1169, #7617 ) ;
#19223=AXIS2_PLACEMENT_3D ( 'NONE', #16574, #14901, #1952 ) ;
#19253=DIRECTION ( 'NONE',  ( -0.000000000000000000, 1.295896757998782163E-15, 1.000000000000000000 ) ) ;
#19314=AXIS2_PLACEMENT_3D ( 'NONE', #623, #13666, #13455 ) ;
#19335=VECTOR ( 'NONE', #19408, 1000.000000000000000 ) ;
#19346=CARTESIAN_POINT ( 'NONE',  ( 5.000000000000000000, 0.000000000000000000, 0.000000000000000000 ) ) ;
#19392=VERTEX_POINT ( 'NONE', #17518 ) ;
#19408=DIRECTION ( 'NONE',  ( 0.000000000000000000, -0.4999999999999987232, 0.8660254037844393737 ) ) ;
#19440=CARTESIAN_POINT ( 'NONE',  ( 0.000000000000000000, -2.342598717236910932, -4.057499999999996554 ) ) ;
#19465=DIRECTION ( 'NONE',  ( 0.000000000000000000, 1.000000000000000000, -1.295896757998782163E-15 ) ) ;
#19467=EDGE_LOOP ( 'NONE', ( #454, #5745, #5741, #16436, #15562 ) ) ;
#19497=LINE ( 'NONE', #7947, #7897 ) ;
#19507=DIRECTION ( 'NONE',  ( 1.000000000000000000, 0.000000000000000000, 0.000000000000000000 ) ) ;
#19625=EDGE_CURVE ( 'NONE', #16672, #2878, #9437, .T. ) ;
#19656=DIRECTION ( 'NONE',  ( 1.000000000000000000, 0.000000000000000000, 0.000000000000000000 ) ) ;
#19705=CARTESIAN_POINT ( 'NONE',  ( 5.000000000000000000, -2.342598717236910932, -4.057499999999996554 ) ) ;
#19745=ORIENTED_EDGE ( 'NONE', *, *, #18111, .F. ) ;
#19774=DIRECTION ( 'NONE',  ( 0.000000000000000000, -1.000000000000000000, 1.110768649713242108E-15 ) ) ;
#19796=LINE ( 'NONE', #302, #15020 ) ;
#19823=EDGE_CURVE ( 'NONE', #18707, #20933, #1070, .T. ) ;
#19841=CARTESIAN_POINT ( 'NONE',  ( 0.000000000000000000, -4.685197434473809430, 6.071532165918824830E-15 ) ) ;
#19842=LINE ( 'NONE', #3946, #5893 ) ;
#19855=ORIENTED_EDGE ( 'NONE', *, *, #10844, .F. ) ;
#19884=ORIENTED_EDGE ( 'NONE', *, *, #17445, .T. ) ;
#19891=AXIS2_PLACEMENT_3D ( 'NONE', #1331, #19134, #1539 ) ;
#19917=DIRECTION ( 'NONE',  ( -1.000000000000000000, -0.000000000000000000, -0.000000000000000000 ) ) ;
#19949=AXIS2_PLACEMENT_3D ( 'NONE', #7967, #4795, #1419 ) ;
#19953=ORIENTED_EDGE ( 'NONE', *, *, #4739, .T. ) ;
#19960=VECTOR ( 'NONE', #19774, 1000.000000000000000 ) ;
#19967=( NAMED_UNIT ( * ) SI_UNIT ( $, .STERADIAN. ) SOLID_ANGLE_UNIT ( ) );
#20015=EDGE_CURVE ( 'NONE', #4158, #6628, #11776, .T. ) ;
#20104=CARTESIAN_POINT ( 'NONE',  ( 0.000000000000000000, 2.342598717236913153, 4.057499999999995666 ) ) ;
#20107=CIRCLE ( 'NONE', #20764, 0.4000000000000001887 ) ;
#20121=ORIENTED_EDGE ( 'NONE', *, *, #1645, .T. ) ;
#20130=ORIENTED_EDGE ( 'NONE', *, *, #5233, .F. ) ;
#20195=FACE_OUTER_BOUND ( 'NONE', #11999, .T. ) ;
#20235=DIRECTION ( 'NONE',  ( -1.000000000000000000, -0.000000000000000000, -0.000000000000000000 ) ) ;
#20275=ADVANCED_FACE ( 'NONE', ( #2820 ), #15857, .T. ) ;
#20281=FACE_OUTER_BOUND ( 'NONE', #19467, .T. ) ;
#20287=EDGE_CURVE ( 'NONE', #18356, #16672, #4608, .T. ) ;
#20306=EDGE_CURVE ( 'NONE', #18834, #8493, #16513, .T. ) ;
#20311=DIRECTION ( 'NONE',  ( 0.000000000000000000, 0.000000000000000000, 1.000000000000000000 ) ) ;
#20347=AXIS2_PLACEMENT_3D ( 'NONE', #19346, #16177, #6817 ) ;
#20365=ADVANCED_FACE ( 'NONE', ( #5213 ), #18064, .F. ) ;
#20419=TOROIDAL_SURFACE ( 'NONE', #20765, 5.400000000000001243, 0.4000000000000000222 ) ;
#20470=CARTESIAN_POINT ( 'NONE',  ( 25.17200000000003612, 6.123233995736767268E-16, -5.000000000000000888 ) ) ;
#20476=AXIS2_PLACEMENT_3D ( 'NONE', #12263, #13962, #15454 ) ;
#20487=DIRECTION ( 'NONE',  ( 0.000000000000000000, -1.224646799147353454E-16, 1.000000000000000000 ) ) ;
#20503=VECTOR ( 'NONE', #14861, 1000.000000000000114 ) ;
#20508=PLANE ( 'NONE',  #4116 ) ;
#20545=EDGE_LOOP ( 'NONE', ( #4434, #4566, #15972, #19953 ) ) ;
#20567=CARTESIAN_POINT ( 'NONE',  ( 5.000000000000000000, 0.000000000000000000, 0.000000000000000000 ) ) ;
#20648=DIRECTION ( 'NONE',  ( 0.000000000000000000, -0.8660254037844393737, -0.4999999999999987232 ) ) ;
#20657=AXIS2_PLACEMENT_3D ( 'NONE', #3634, #10194, #13301 ) ;
#20659=LINE ( 'NONE', #14432, #11451 ) ;
#20709=LINE ( 'NONE', #5966, #17541 ) ;
#20764=AXIS2_PLACEMENT_3D ( 'NONE', #15706, #15596, #15498 ) ;
#20765=AXIS2_PLACEMENT_3D ( 'NONE', #11267, #19507, #6566 ) ;
#20799=ORIENTED_EDGE ( 'NONE', *, *, #14721, .T. ) ;
#20805=ORIENTED_EDGE ( 'NONE', *, *, #3899, .F. ) ;
#20824=VECTOR ( 'NONE', #17279, 1000.000000000000000 ) ;
#20828=CLOSED_SHELL ( 'NONE', ( #9530, #3168, #4628, #15128, #15548, #1734, #13070, #1398, #8039, #2877, #822, #16909, #13438, #6252, #16904, #393, #20275, #11226, #15216, #5038, #9427, #20365, #6354, #3475, #293, #7591, #14577 ) ) ;
#20893=AXIS2_PLACEMENT_3D ( 'NONE', #2730, #7485, #13978 ) ;
#20894=DIRECTION ( 'NONE',  ( 1.000000000000000000, 0.000000000000000000, 0.000000000000000000 ) ) ;
#20933=VERTEX_POINT ( 'NONE', #12617 ) ;
#20989=COLOUR_RGB('Black',0.12,0.14,0.17);
#20990=FILL_AREA_STYLE_COLOUR('',#20989);
#20991=FILL_AREA_STYLE('',(#20990));
#20992=SURFACE_STYLE_FILL_AREA(#20991);
#20993=SURFACE_SIDE_STYLE('',(#20992));
#20994=SURFACE_STYLE_USAGE(.BOTH.,#20993);
#20995=PRESENTATION_STYLE_ASSIGNMENT((#20994));
ENDSEC;
END-ISO-10303-21;
